ISO-10303-21;
HEADER;
FILE_DESCRIPTION (('STEP AP214'),
    '1' );
FILE_NAME ('Nut.step',
    '2026-10-24T18:16:00',
    ( '' ),
    ( '' ),
    'SwSTEP 2.0',
    'SolidWorks 2025',
    '' );
FILE_SCHEMA (( 'AUTOMOTIVE_DESIGN' ));
ENDSEC;

DATA;
#14=LINE ( 'NONE', #82, #14399 ) ;
#82=CARTESIAN_POINT ( 'NONE',  ( -0.09061599198715356018, 0.07874015748031495954, -0.007444810018878696839 ) ) ;
#90=EDGE_LOOP ( 'NONE', ( #14793, #1805, #11512, #7748 ) ) ;
#100=CARTESIAN_POINT ( 'NONE',  ( -0.04748649982359137017, 0.06963377358818916008, -0.06973926505268103482 ) ) ;
#146=AXIS2_PLACEMENT_3D ( 'NONE', #6930, #11726, #4572 ) ;
#161=VERTEX_POINT ( 'NONE', #8231 ) ;
#238=VERTEX_POINT ( 'NONE', #12837 ) ;
#250=ADVANCED_FACE ( 'NONE', ( #14021 ), #3364, .F. ) ;
#306=ADVANCED_FACE ( 'NONE', ( #3682 ), #9787, .F. ) ;
#331=CARTESIAN_POINT ( 'NONE',  ( -0.07118569129171407883, 0.07239639532897743091, 0.03365426801084205055 ) ) ;
#415=ORIENTED_EDGE ( 'NONE', *, *, #6850, .T. ) ;
#428=EDGE_CURVE ( 'NONE', #2378, #3129, #9650, .T. ) ;
#470=EDGE_LOOP ( 'NONE', ( #2479, #415, #5574, #10167, #3437 ) ) ;
#476=LINE ( 'NONE', #5221, #628 ) ;
#608=ADVANCED_FACE ( 'NONE', ( #9364 ), #6879, .T. ) ;
#611=VECTOR ( 'NONE', #11502, 39.37007874015748143 ) ;
#628=VECTOR ( 'NONE', #11097, 39.37007874015748854 ) ;
#665=CARTESIAN_POINT ( 'NONE',  ( 0.05175539059627461136, 0.06736074103232447818, -0.07475334604056278753 ) ) ;
#685=DIRECTION ( 'NONE',  ( -0.5692328345973367565, 0.000000000000000000, 0.8221763679505029732 ) ) ;
#699=CARTESIAN_POINT ( 'NONE',  ( 0.02590706759391969358, 0.06931031770563803041, 0.08113392229587690352 ) ) ;
#735=ORIENTED_EDGE ( 'NONE', *, *, #5267, .F. ) ;
#745=DIRECTION ( 'NONE',  ( -0.000000000000000000, -1.000000000000000000, -0.000000000000000000 ) ) ;
#755=CARTESIAN_POINT ( 'NONE',  ( 0.03886060139087953863, 0.07874015748031495954, 0.08219815605943972536 ) ) ;
#800=CARTESIAN_POINT ( 'NONE',  ( 9.360245101547351149E-18, 0.07093549527207514138, 0.07900545476875124595 ) ) ;
#832=ORIENTED_EDGE ( 'NONE', *, *, #3269, .F. ) ;
#847=ADVANCED_FACE ( 'NONE', ( #10281, #4174 ), #15060, .T. ) ;
#854=AXIS2_PLACEMENT_3D ( 'NONE', #12975, #4803, #3424 ) ;
#912=( LENGTH_UNIT ( ) NAMED_UNIT ( * ) SI_UNIT ( $, .METRE. ) );
#914=PRODUCT_DEFINITION_SHAPE ( 'NONE', 'NONE',  #6099 ) ;
#917=CARTESIAN_POINT ( 'NONE',  ( 4.821444091131316146E-18, 0.07480314960629921850, 0.03937007874015751446 ) ) ;
#921=STYLED_ITEM('',(#15533),#9543);
#951=CIRCLE ( 'NONE', #15455, 0.003937007874015749712 ) ;
#994=( NAMED_UNIT ( * ) PLANE_ANGLE_UNIT ( ) SI_UNIT ( $, .RADIAN. ) );
#996=CARTESIAN_POINT ( 'NONE',  ( 0.03886060139087953863, 0.000000000000000000, 0.08219815605943972536 ) ) ;
#1004=VERTEX_POINT ( 'NONE', #800 ) ;
#1047=LINE ( 'NONE', #11852, #8451 ) ;
#1104=APPLICATION_CONTEXT ( 'automotive_design' ) ;
#1112=ORIENTED_EDGE ( 'NONE', *, *, #1196, .F. ) ;
#1184=EDGE_CURVE ( 'NONE', #2378, #12957, #5055, .T. ) ;
#1196=EDGE_CURVE ( 'NONE', #10513, #12909, #476, .T. ) ;
#1228=PLANE ( 'NONE',  #854 ) ;
#1292=CARTESIAN_POINT ( 'NONE',  ( 0.000000000000000000, 0.003937007874015749712, 0.04330708661417326938 ) ) ;
#1341=CARTESIAN_POINT ( 'NONE',  ( -0.03886060139087894189, 0.06736074103232447818, -0.08219815605944147396 ) ) ;
#1396=DIRECTION ( 'NONE',  ( 0.4274092037376936992, 0.000000000000000000, 0.9040582794047684612 ) ) ;
#1451=DIRECTION ( 'NONE',  ( 0.000000000000000000, 0.000000000000000000, 1.000000000000000000 ) ) ;
#1622=DIRECTION ( 'NONE',  ( -0.08188191145426276796, 0.000000000000000000, 0.9966420383350264034 ) ) ;
#1636=DIRECTION ( 'NONE',  ( 0.000000000000000000, 0.000000000000000000, -1.000000000000000000 ) ) ;
#1654=ORIENTED_EDGE ( 'NONE', *, *, #1746, .T. ) ;
#1661=CARTESIAN_POINT ( 'NONE',  ( -0.08199009355444111802, 0.06963377358818916008, -0.01990370102563917068 ) ) ;
#1676=ORIENTED_EDGE ( 'NONE', *, *, #1937, .F. ) ;
#1727=ORIENTED_EDGE ( 'NONE', *, *, #428, .F. ) ;
#1746=EDGE_CURVE ( 'NONE', #12957, #11239, #3028, .T. ) ;
#1789=LINE ( 'NONE', #10248, #611 ) ;
#1805=ORIENTED_EDGE ( 'NONE', *, *, #14342, .F. ) ;
#1818=CARTESIAN_POINT ( 'NONE',  ( 2.419703784132994590E-19, 0.07093549527207483607, -0.07900545476875228679 ) ) ;
#1838=CARTESIAN_POINT ( 'NONE',  ( -0.09061599198715356018, 0.06736074103232447818, -0.007444810018878696839 ) ) ;
#1839=DIRECTION ( 'NONE',  ( -0.000000000000000000, -1.000000000000000000, -0.000000000000000000 ) ) ;
#1840=B_SPLINE_CURVE_WITH_KNOTS ( 'NONE', 3,
 ( #7392, #6441, #5185, #3869 ),
 .UNSPECIFIED., .F., .F.,
 ( 4, 4 ),
 ( 2.006738551125145802E-07, 0.0009905856238791850652 ),
 .UNSPECIFIED. ) ;
#1845=AXIS2_PLACEMENT_3D ( 'NONE', #10153, #13513, #11403 ) ;
#1856=EDGE_CURVE ( 'NONE', #3129, #1004, #1047, .T. ) ;
#1903=CONICAL_SURFACE ( 'NONE', #11919, 0.05298991407461853265, 1.279339532317029349 ) ;
#1937=EDGE_CURVE ( 'NONE', #7178, #3700, #13839, .T. ) ;
#1943=EDGE_CURVE ( 'NONE', #4794, #8918, #951, .T. ) ;
#2055=CARTESIAN_POINT ( 'NONE',  ( 0.000000000000000000, 0.003937007874015749712, 0.000000000000000000 ) ) ;
#2068=LINE ( 'NONE', #6842, #11331 ) ;
#2072=EDGE_CURVE ( 'NONE', #3129, #2378, #9497, .T. ) ;
#2124=ADVANCED_FACE ( 'NONE', ( #3823 ), #14119, .T. ) ;
#2159=AXIS2_PLACEMENT_3D ( 'NONE', #10514, #4404, #6745 ) ;
#2239=SHAPE_REPRESENTATION_RELATIONSHIP ( 'NONE' , 'NONE' ,  #2403, #3470 ) ;
#2260=CARTESIAN_POINT ( 'NONE',  ( -0.05175539059627463218, 0.06736074103232447818, 0.07475334604056275978 ) ) ;
#2312=VERTEX_POINT ( 'NONE', #5225 ) ;
#2365=EDGE_CURVE ( 'NONE', #161, #13241, #9085, .T. ) ;
#2378=VERTEX_POINT ( 'NONE', #3562 ) ;
#2380=ORIENTED_EDGE ( 'NONE', *, *, #4251, .F. ) ;
#2403=SHAPE_REPRESENTATION ( 'Nut', ( #11481 ), #7714 ) ;
#2466=ORIENTED_EDGE ( 'NONE', *, *, #428, .T. ) ;
#2479=ORIENTED_EDGE ( 'NONE', *, *, #4908, .F. ) ;
#2517=DIRECTION ( 'NONE',  ( 0.000000000000000000, 0.000000000000000000, 1.000000000000000000 ) ) ;
#2546=ADVANCED_FACE ( 'NONE', ( #7943 ), #4839, .T. ) ;
#2614=DIRECTION ( 'NONE',  ( -0.000000000000000000, -1.000000000000000000, -0.000000000000000000 ) ) ;
#2620=VECTOR ( 'NONE', #6510, 39.37007874015748854 ) ;
#2713=EDGE_CURVE ( 'NONE', #12588, #7178, #3574, .T. ) ;
#2744=ORIENTED_EDGE ( 'NONE', *, *, #11806, .F. ) ;
#2778=DIRECTION ( 'NONE',  ( -0.8221763679505030842, 0.000000000000000000, -0.5692328345973368675 ) ) ;
#2793=CARTESIAN_POINT ( 'NONE',  ( 0.000000000000000000, 0.07874015748031495954, -0.05298991407461853265 ) ) ;
#2796=CARTESIAN_POINT ( 'NONE',  ( 0.09061599198715353243, 0.000000000000000000, 0.007444810018878659542 ) ) ;
#2845=AXIS2_PLACEMENT_3D ( 'NONE', #1292, #7241, #1451 ) ;
#2873=AXIS2_PLACEMENT_3D ( 'NONE', #13466, #8689, #1636 ) ;
#2951=TOROIDAL_SURFACE ( 'NONE', #3457, 0.04330708661417326938, 0.003937007874015747977 ) ;
#2981=UNCERTAINTY_MEASURE_WITH_UNIT (LENGTH_MEASURE( 1.000000000000000082E-05 ), #15165, 'distance_accuracy_value', 'NONE');
#3028=B_SPLINE_CURVE_WITH_KNOTS ( 'NONE', 3,
 ( #1818, #12644, #11385, #665 ),
 .UNSPECIFIED., .F., .F.,
 ( 4, 4 ),
 ( 0.0009905856238791850652, 0.002309601750613615636 ),
 .UNSPECIFIED. ) ;
#3041=LINE ( 'NONE', #4136, #5588 ) ;
#3101=DIRECTION ( 'NONE',  ( -0.9966420383350279577, 0.000000000000000000, -0.08188191145424326967 ) ) ;
#3129=VERTEX_POINT ( 'NONE', #7816 ) ;
#3226=DIRECTION ( 'NONE',  ( 0.000000000000000000, 0.000000000000000000, -1.000000000000000000 ) ) ;
#3232=CARTESIAN_POINT ( 'NONE',  ( 0.09061599198715353243, 0.07874015748031495954, 0.007444810018878659542 ) ) ;
#3269=EDGE_CURVE ( 'NONE', #7658, #10513, #8288, .T. ) ;
#3301=B_SPLINE_CURVE_WITH_KNOTS ( 'NONE', 3,
 ( #8539, #11263, #7892, #13315, #14872 ),
 .UNSPECIFIED., .F., .F.,
 ( 4, 1, 4 ),
 ( 2.212246760591329979E-07, 0.001154921763055310720, 0.002309622301434562531 ),
 .UNSPECIFIED. ) ;
#3302=EDGE_LOOP ( 'NONE', ( #832, #3932, #4443, #14506, #735, #1112 ) ) ;
#3311=ORIENTED_EDGE ( 'NONE', *, *, #2713, .T. ) ;
#3364=PLANE ( 'NONE',  #14382 ) ;
#3370=VECTOR ( 'NONE', #10814, 39.37007874015748143 ) ;
#3410=EDGE_LOOP ( 'NONE', ( #5694, #11551 ) ) ;
#3424=DIRECTION ( 'NONE',  ( 0.5692328345973325376, 0.000000000000000000, -0.8221763679505059708 ) ) ;
#3437=ORIENTED_EDGE ( 'NONE', *, *, #3269, .T. ) ;
#3439=AXIS2_PLACEMENT_3D ( 'NONE', #3232, #11602, #14109 ) ;
#3457=AXIS2_PLACEMENT_3D ( 'NONE', #6936, #12895, #2517 ) ;
#3460=CYLINDRICAL_SURFACE ( 'NONE', #15439, 0.03937007874015751446 ) ;
#3470=ADVANCED_BREP_SHAPE_REPRESENTATION ( '', ( #9543, #11481 ), #7714 ) ;
#3551=ORIENTED_EDGE ( 'NONE', *, *, #4251, .T. ) ;
#3562=CARTESIAN_POINT ( 'NONE',  ( 0.000000000000000000, 0.07874015748031495954, -0.05298991407461853265 ) ) ;
#3574=B_SPLINE_CURVE_WITH_KNOTS ( 'NONE', 3,
 ( #11047, #14582, #331, #8717, #5169 ),
 .UNSPECIFIED., .F., .F.,
 ( 4, 1, 4 ),
 ( 2.212246760591329979E-07, 0.001154921763055310937, 0.002309622301434562965 ),
 .UNSPECIFIED. ) ;
#3628=CARTESIAN_POINT ( 'NONE',  ( 0.000000000000000000, 0.07874015748031495954, -0.03937007874015751446 ) ) ;
#3682=FACE_OUTER_BOUND ( 'NONE', #3816, .T. ) ;
#3700=VERTEX_POINT ( 'NONE', #10705 ) ;
#3751=EDGE_LOOP ( 'NONE', ( #5283, #11890, #7544, #7950 ) ) ;
#3816=EDGE_LOOP ( 'NONE', ( #7841, #5554, #8593, #9327 ) ) ;
#3823=FACE_OUTER_BOUND ( 'NONE', #4275, .T. ) ;
#3829=DIRECTION ( 'NONE',  ( -1.000000000000000000, -0.000000000000000000, 0.000000000000000000 ) ) ;
#3846=ORIENTED_EDGE ( 'NONE', *, *, #9108, .F. ) ;
#3869=CARTESIAN_POINT ( 'NONE',  ( 2.419703784132994590E-19, 0.07093549527207483607, -0.07900545476875228679 ) ) ;
#3891=CONICAL_SURFACE ( 'NONE', #11647, 0.05298991407461853265, 1.279339532317029349 ) ;
#3932=ORIENTED_EDGE ( 'NONE', *, *, #6134, .F. ) ;
#3981=DIRECTION ( 'NONE',  ( 0.000000000000000000, 0.000000000000000000, -1.000000000000000000 ) ) ;
#4038=FACE_OUTER_BOUND ( 'NONE', #9060, .T. ) ;
#4136=CARTESIAN_POINT ( 'NONE',  ( -0.03886060139087894189, 0.000000000000000000, -0.08219815605944147396 ) ) ;
#4149=ADVANCED_FACE ( 'NONE', ( #10538 ), #1228, .F. ) ;
#4174=FACE_OUTER_BOUND ( 'NONE', #14256, .T. ) ;
#4244=EDGE_CURVE ( 'NONE', #3700, #12957, #1840, .T. ) ;
#4251=EDGE_CURVE ( 'NONE', #11239, #4631, #13346, .T. ) ;
#4252=CARTESIAN_POINT ( 'NONE',  ( 0.09061599198715353243, 0.000000000000000000, 0.007444810018878659542 ) ) ;
#4264=DIRECTION ( 'NONE',  ( 0.000000000000000000, 0.000000000000000000, 1.000000000000000000 ) ) ;
#4275=EDGE_LOOP ( 'NONE', ( #5762, #5595, #14067, #12885 ) ) ;
#4311=DIRECTION ( 'NONE',  ( -0.000000000000000000, 1.000000000000000000, 0.000000000000000000 ) ) ;
#4322=AXIS2_PLACEMENT_3D ( 'NONE', #10962, #9725, #9868 ) ;
#4398=CIRCLE ( 'NONE', #11150, 0.04330708661417326938 ) ;
#4404=DIRECTION ( 'NONE',  ( 0.000000000000000000, -1.000000000000000000, -0.000000000000000000 ) ) ;
#4440=ORIENTED_EDGE ( 'NONE', *, *, #6473, .F. ) ;
#4443=ORIENTED_EDGE ( 'NONE', *, *, #4904, .F. ) ;
#4453=DIRECTION ( 'NONE',  ( -0.000000000000000000, -1.000000000000000000, -0.000000000000000000 ) ) ;
#4454=CARTESIAN_POINT ( 'NONE',  ( 5.303588500244448531E-18, 0.07874015748031495954, -0.04330708661417326938 ) ) ;
#4491=DIRECTION ( 'NONE',  ( -0.000000000000000000, 1.000000000000000000, 0.000000000000000000 ) ) ;
#4512=ORIENTED_EDGE ( 'NONE', *, *, #1184, .F. ) ;
#4521=DIRECTION ( 'NONE',  ( 0.000000000000000000, 0.000000000000000000, -1.000000000000000000 ) ) ;
#4527=CARTESIAN_POINT ( 'NONE',  ( -0.01725179686542488086, 0.07136070614489399555, 0.07758808519268840798 ) ) ;
#4531=ORIENTED_EDGE ( 'NONE', *, *, #11806, .T. ) ;
#4551=EDGE_LOOP ( 'NONE', ( #7817, #6345, #4531, #9521 ) ) ;
#4572=DIRECTION ( 'NONE',  ( 0.000000000000000000, 0.000000000000000000, 1.000000000000000000 ) ) ;
#4597=CARTESIAN_POINT ( 'NONE',  ( 0.05175539059627461136, 0.06736074103232447818, -0.07475334604056278753 ) ) ;
#4602=DIRECTION ( 'NONE',  ( 0.9966420383350279577, 0.000000000000000000, 0.08188191145424326967 ) ) ;
#4622=CIRCLE ( 'NONE', #7124, 0.03937007874015751446 ) ;
#4631=VERTEX_POINT ( 'NONE', #10731 ) ;
#4788=CARTESIAN_POINT ( 'NONE',  ( 0.000000000000000000, 8.003460918938271148E-19, 0.04330708661417326938 ) ) ;
#4794=VERTEX_POINT ( 'NONE', #6169 ) ;
#4803=DIRECTION ( 'NONE',  ( 0.8221763679505059708, -0.000000000000000000, 0.5692328345973325376 ) ) ;
#4839=TOROIDAL_SURFACE ( 'NONE', #12350, 0.04330708661417326938, 0.003937007874015747977 ) ;
#4841=DIRECTION ( 'NONE',  ( -0.000000000000000000, -1.000000000000000000, -0.000000000000000000 ) ) ;
#4867=CARTESIAN_POINT ( 'NONE',  ( 5.303588500244447761E-18, 0.003937007874015749712, -0.04330708661417326938 ) ) ;
#4904=EDGE_CURVE ( 'NONE', #9513, #238, #3041, .T. ) ;
#4908=EDGE_CURVE ( 'NONE', #14540, #10513, #1789, .T. ) ;
#5003=ORIENTED_EDGE ( 'NONE', *, *, #11748, .T. ) ;
#5029=PRODUCT ( 'Nut', 'Nut', '', ( #5253 ) ) ;
#5055=LINE ( 'NONE', #2793, #14380 ) ;
#5075=ORIENTED_EDGE ( 'NONE', *, *, #1856, .F. ) ;
#5094=DIRECTION ( 'NONE',  ( 1.224646799147353207E-16, 0.000000000000000000, -1.000000000000000000 ) ) ;
#5122=ORIENTED_EDGE ( 'NONE', *, *, #2713, .F. ) ;
#5169=CARTESIAN_POINT ( 'NONE',  ( -0.09061599198715356018, 0.06736074103232447818, -0.007444810018878696839 ) ) ;
#5183=CARTESIAN_POINT ( 'NONE',  ( -0.05175539059627463218, 0.000000000000000000, 0.07475334604056275978 ) ) ;
#5185=CARTESIAN_POINT ( 'NONE',  ( -0.01295353379695964903, 0.07061622514300590348, -0.08006968853231534455 ) ) ;
#5207=DIRECTION ( 'NONE',  ( -0.000000000000000000, 1.000000000000000000, 0.000000000000000000 ) ) ;
#5209=CARTESIAN_POINT ( 'NONE',  ( 0.05175539059627461136, 0.07874015748031495954, -0.07475334604056278753 ) ) ;
#5221=CARTESIAN_POINT ( 'NONE',  ( 0.03886060139087953863, 0.000000000000000000, 0.08219815605943972536 ) ) ;
#5225=CARTESIAN_POINT ( 'NONE',  ( 0.000000000000000000, 0.07874015748031495954, 0.04330708661417326938 ) ) ;
#5253=PRODUCT_CONTEXT ( 'NONE', #1104, 'mechanical' ) ;
#5267=EDGE_CURVE ( 'NONE', #12909, #4631, #11233, .T. ) ;
#5283=ORIENTED_EDGE ( 'NONE', *, *, #8253, .F. ) ;
#5362=DIRECTION ( 'NONE',  ( -0.000000000000000000, 1.000000000000000000, 0.000000000000000000 ) ) ;
#5378=DIRECTION ( 'NONE',  ( -0.5692328345973325376, 0.000000000000000000, 0.8221763679505059708 ) ) ;
#5410=FACE_OUTER_BOUND ( 'NONE', #10674, .T. ) ;
#5441=DIRECTION ( 'NONE',  ( 1.000000000000000000, 0.000000000000000000, 0.000000000000000000 ) ) ;
#5442=AXIS2_PLACEMENT_3D ( 'NONE', #755, #2778, #685 ) ;
#5444=DIRECTION ( 'NONE',  ( 0.000000000000000000, 0.000000000000000000, 1.000000000000000000 ) ) ;
#5447=FACE_OUTER_BOUND ( 'NONE', #470, .T. ) ;
#5456=CARTESIAN_POINT ( 'NONE',  ( 0.01295353379695985026, 0.07061622514300630593, 0.08006968853231406780 ) ) ;
#5480=ORIENTED_EDGE ( 'NONE', *, *, #1184, .T. ) ;
#5501=EDGE_CURVE ( 'NONE', #161, #4794, #10684, .T. ) ;
#5548=VERTEX_POINT ( 'NONE', #4788 ) ;
#5554=ORIENTED_EDGE ( 'NONE', *, *, #8253, .T. ) ;
#5574=ORIENTED_EDGE ( 'NONE', *, *, #8763, .T. ) ;
#5576=AXIS2_PLACEMENT_3D ( 'NONE', #11797, #15402, #13990 ) ;
#5577=EDGE_LOOP ( 'NONE', ( #10457, #3311, #5914, #8965 ) ) ;
#5582=PLANE ( 'NONE',  #5576 ) ;
#5588=VECTOR ( 'NONE', #5378, 39.37007874015748143 ) ;
#5589=CARTESIAN_POINT ( 'NONE',  ( 0.03886060139087953863, 0.06736074103232488064, 0.08219815605943972536 ) ) ;
#5595=ORIENTED_EDGE ( 'NONE', *, *, #8189, .F. ) ;
#5694=ORIENTED_EDGE ( 'NONE', *, *, #14342, .T. ) ;
#5762=ORIENTED_EDGE ( 'NONE', *, *, #1943, .F. ) ;
#5764=CARTESIAN_POINT ( 'NONE',  ( -0.05175539059627463218, 0.000000000000000000, 0.07475334604056275978 ) ) ;
#5765=CARTESIAN_POINT ( 'NONE',  ( 9.360245101547351149E-18, 0.07093549527207514138, 0.07900545476875124595 ) ) ;
#5804=EDGE_LOOP ( 'NONE', ( #7052, #12741, #10671, #11361 ) ) ;
#5829=CIRCLE ( 'NONE', #1845, 0.03937007874015751446 ) ;
#5903=B_SPLINE_CURVE_WITH_KNOTS ( 'NONE', 3,
 ( #11422, #699, #5456, #10245 ),
 .UNSPECIFIED., .F., .F.,
 ( 4, 4 ),
 ( 2.006738551125145802E-07, 0.0009905856238791982925 ),
 .UNSPECIFIED. ) ;
#5910=DIRECTION ( 'NONE',  ( 0.000000000000000000, 0.000000000000000000, 1.000000000000000000 ) ) ;
#5914=ORIENTED_EDGE ( 'NONE', *, *, #12751, .T. ) ;
#5939=DIRECTION ( 'NONE',  ( -0.000000000000000000, -1.000000000000000000, -0.000000000000000000 ) ) ;
#5971=ORIENTED_EDGE ( 'NONE', *, *, #6776, .T. ) ;
#5986=APPLICATION_CONTEXT ( 'automotive_design' ) ;
#6035=DIRECTION ( 'NONE',  ( 1.000000000000000000, 0.000000000000000000, 1.224646799147353207E-16 ) ) ;
#6049=DIRECTION ( 'NONE',  ( -0.000000000000000000, 1.000000000000000000, 0.000000000000000000 ) ) ;
#6065=VECTOR ( 'NONE', #1839, 39.37007874015748143 ) ;
#6099=PRODUCT_DEFINITION ( 'UNKNOWN', '', #6856, #11442 ) ;
#6129=AXIS2_PLACEMENT_3D ( 'NONE', #5209, #1622, #14547 ) ;
#6134=EDGE_CURVE ( 'NONE', #238, #7658, #14632, .T. ) ;
#6152=ADVANCED_FACE ( 'NONE', ( #4038 ), #6465, .F. ) ;
#6158=DIRECTION ( 'NONE',  ( -0.000000000000000000, -1.000000000000000000, -0.000000000000000000 ) ) ;
#6169=CARTESIAN_POINT ( 'NONE',  ( 0.000000000000000000, 0.003937007874015749712, -0.03937007874015751446 ) ) ;
#6176=CARTESIAN_POINT ( 'NONE',  ( 0.000000000000000000, 0.07480314960629921850, 0.04330708661417326938 ) ) ;
#6192=EDGE_LOOP ( 'NONE', ( #12257, #7802, #10182, #10306 ) ) ;
#6265=ORIENTED_EDGE ( 'NONE', *, *, #11716, .T. ) ;
#6289=CARTESIAN_POINT ( 'NONE',  ( -0.09061599198715356018, 0.000000000000000000, -0.007444810018878696839 ) ) ;
#6298=EDGE_CURVE ( 'NONE', #10074, #14540, #11344, .T. ) ;
#6301=ADVANCED_FACE ( 'NONE', ( #5447 ), #15020, .F. ) ;
#6345=ORIENTED_EDGE ( 'NONE', *, *, #1937, .T. ) ;
#6378=PLANE ( 'NONE',  #5442 ) ;
#6441=CARTESIAN_POINT ( 'NONE',  ( -0.02590706759391929112, 0.06931031770563762795, -0.08113392229587841620 ) ) ;
#6465=PLANE ( 'NONE',  #6129 ) ;
#6473=EDGE_CURVE ( 'NONE', #4794, #6904, #12915, .T. ) ;
#6510=DIRECTION ( 'NONE',  ( -0.4274092037376938102, 0.000000000000000000, -0.9040582794047684612 ) ) ;
#6590=CARTESIAN_POINT ( 'NONE',  ( 0.000000000000000000, 0.003937007874015749712, 0.000000000000000000 ) ) ;
#6611=CARTESIAN_POINT ( 'NONE',  ( 0.06473829668901658063, 0.07239639532902293617, 0.04482148303915918508 ) ) ;
#6644=( GEOMETRIC_REPRESENTATION_CONTEXT ( 3 ) GLOBAL_UNCERTAINTY_ASSIGNED_CONTEXT ( ( #14747 ) ) GLOBAL_UNIT_ASSIGNED_CONTEXT ( ( #9518, #14370, #9277 ) ) REPRESENTATION_CONTEXT ( 'NONE', 'WORKASPACE' ) );
#6688=DIRECTION ( 'NONE',  ( 0.000000000000000000, 0.000000000000000000, 1.000000000000000000 ) ) ;
#6745=DIRECTION ( 'NONE',  ( 0.000000000000000000, 0.000000000000000000, 1.000000000000000000 ) ) ;
#6776=EDGE_CURVE ( 'NONE', #11239, #10074, #3301, .T. ) ;
#6788=LINE ( 'NONE', #7691, #14913 ) ;
#6842=CARTESIAN_POINT ( 'NONE',  ( -0.03886060139087894189, 0.07874015748031495954, -0.08219815605944147396 ) ) ;
#6850=EDGE_CURVE ( 'NONE', #14540, #1004, #5903, .T. ) ;
#6856=PRODUCT_DEFINITION_FORMATION_WITH_SPECIFIED_SOURCE ( 'ANY', '', #5029, .NOT_KNOWN. ) ;
#6879=TOROIDAL_SURFACE ( 'NONE', #146, 0.04330708661417326938, 0.003937007874015747977 ) ;
#6884=CARTESIAN_POINT ( 'NONE',  ( -0.09061599198715356018, 0.07874015748031495954, -0.007444810018878696839 ) ) ;
#6904=VERTEX_POINT ( 'NONE', #8128 ) ;
#6930=CARTESIAN_POINT ( 'NONE',  ( 0.000000000000000000, 0.07480314960629921850, 0.000000000000000000 ) ) ;
#6936=CARTESIAN_POINT ( 'NONE',  ( 0.000000000000000000, 0.07480314960629921850, 0.000000000000000000 ) ) ;
#6961=DIRECTION ( 'NONE',  ( 0.000000000000000000, -1.000000000000000000, -0.000000000000000000 ) ) ;
#7026=LINE ( 'NONE', #9300, #15199 ) ;
#7033=CARTESIAN_POINT ( 'NONE',  ( 0.03886060139087953863, 0.06736074103232488064, 0.08219815605943972536 ) ) ;
#7052=ORIENTED_EDGE ( 'NONE', *, *, #11748, .F. ) ;
#7117=CARTESIAN_POINT ( 'NONE',  ( 0.000000000000000000, 0.07874015748031495954, 0.000000000000000000 ) ) ;
#7124=AXIS2_PLACEMENT_3D ( 'NONE', #6590, #7624, #12420 ) ;
#7177=CIRCLE ( 'NONE', #13931, 0.003937007874015749712 ) ;
#7178=VERTEX_POINT ( 'NONE', #1838 ) ;
#7232=EDGE_CURVE ( 'NONE', #13241, #161, #5829, .T. ) ;
#7236=AXIS2_PLACEMENT_3D ( 'NONE', #10426, #10733, #9559 ) ;
#7241=DIRECTION ( 'NONE',  ( -1.000000000000000000, -0.000000000000000000, 0.000000000000000000 ) ) ;
#7247=CARTESIAN_POINT ( 'NONE',  ( 0.000000000000000000, 0.07480314960629921850, 0.000000000000000000 ) ) ;
#7315=ADVANCED_FACE ( 'NONE', ( #8106, #15315 ), #5582, .F. ) ;
#7335=ORIENTED_EDGE ( 'NONE', *, *, #9108, .T. ) ;
#7392=CARTESIAN_POINT ( 'NONE',  ( -0.03886060139087894189, 0.06736074103232447818, -0.08219815605944147396 ) ) ;
#7444=EDGE_CURVE ( 'NONE', #11304, #2312, #14614, .T. ) ;
#7493=FACE_OUTER_BOUND ( 'NONE', #12181, .T. ) ;
#7517=EDGE_CURVE ( 'NONE', #6904, #5548, #9107, .T. ) ;
#7539=LINE ( 'NONE', #11390, #10131 ) ;
#7544=ORIENTED_EDGE ( 'NONE', *, *, #5501, .T. ) ;
#7624=DIRECTION ( 'NONE',  ( 0.000000000000000000, -1.000000000000000000, -0.000000000000000000 ) ) ;
#7658=VERTEX_POINT ( 'NONE', #5183 ) ;
#7691=CARTESIAN_POINT ( 'NONE',  ( 0.05175539059627461136, 0.000000000000000000, -0.07475334604056278753 ) ) ;
#7714=( GEOMETRIC_REPRESENTATION_CONTEXT ( 3 ) GLOBAL_UNCERTAINTY_ASSIGNED_CONTEXT ( ( #2981 ) ) GLOBAL_UNIT_ASSIGNED_CONTEXT ( ( #15165, #994, #15246 ) ) REPRESENTATION_CONTEXT ( 'NONE', 'WORKASPACE' ) );
#7733=ORIENTED_EDGE ( 'NONE', *, *, #1856, .T. ) ;
#7748=ORIENTED_EDGE ( 'NONE', *, *, #2365, .F. ) ;
#7793=CARTESIAN_POINT ( 'NONE',  ( 0.08199009355444122904, 0.06963377358818914620, 0.01990370102563883067 ) ) ;
#7802=ORIENTED_EDGE ( 'NONE', *, *, #9695, .T. ) ;
#7816=CARTESIAN_POINT ( 'NONE',  ( 8.825956286652729502E-18, 0.07874015748031495954, 0.05298991407461853265 ) ) ;
#7817=ORIENTED_EDGE ( 'NONE', *, *, #12751, .F. ) ;
#7841=ORIENTED_EDGE ( 'NONE', *, *, #2365, .T. ) ;
#7892=CARTESIAN_POINT ( 'NONE',  ( 0.07118569129171406495, 0.07239639532897740315, -0.03365426801084208525 ) ) ;
#7943=FACE_OUTER_BOUND ( 'NONE', #9225, .T. ) ;
#7950=ORIENTED_EDGE ( 'NONE', *, *, #6473, .T. ) ;
#7965=EDGE_LOOP ( 'NONE', ( #5075, #14684, #5480, #11833, #1676, #5122, #13966 ) ) ;
#8040=CARTESIAN_POINT ( 'NONE',  ( 0.09061599198715353243, 0.06736074103232449206, 0.007444810018878659542 ) ) ;
#8049=DIRECTION ( 'NONE',  ( -0.9966420383350262924, 0.000000000000000000, -0.08188191145426275408 ) ) ;
#8106=FACE_BOUND ( 'NONE', #11564, .T. ) ;
#8128=CARTESIAN_POINT ( 'NONE',  ( 4.821444091131316146E-18, 0.003937007874015749712, 0.03937007874015751446 ) ) ;
#8146=DIRECTION ( 'NONE',  ( -0.4274092037376936992, 0.000000000000000000, -0.9040582794047685722 ) ) ;
#8189=EDGE_CURVE ( 'NONE', #6904, #4794, #4622, .T. ) ;
#8231=CARTESIAN_POINT ( 'NONE',  ( 0.000000000000000000, 0.07480314960629921850, -0.03937007874015751446 ) ) ;
#8238=CARTESIAN_POINT ( 'NONE',  ( 0.000000000000000000, 0.07874015748031495954, 0.000000000000000000 ) ) ;
#8253=EDGE_CURVE ( 'NONE', #13241, #6904, #7539, .T. ) ;
#8288=LINE ( 'NONE', #5764, #9863 ) ;
#8451=VECTOR ( 'NONE', #15299, 39.37007874015748854 ) ;
#8456=ORIENTED_EDGE ( 'NONE', *, *, #2072, .F. ) ;
#8539=CARTESIAN_POINT ( 'NONE',  ( 0.05175539059627461136, 0.06736074103232447818, -0.07475334604056278753 ) ) ;
#8591=CARTESIAN_POINT ( 'NONE',  ( 5.303588500244448531E-18, 8.003460918938271148E-19, -0.04330708661417326938 ) ) ;
#8593=ORIENTED_EDGE ( 'NONE', *, *, #8189, .T. ) ;
#8616=ORIENTED_EDGE ( 'NONE', *, *, #6850, .F. ) ;
#8624=CLOSED_SHELL ( 'NONE', ( #608, #2546, #8969, #306, #847, #7315, #6301, #10278, #9788, #6152, #4149, #250, #14138, #12990, #2124, #10394 ) ) ;
#8673=CARTESIAN_POINT ( 'NONE',  ( 0.000000000000000000, 0.000000000000000000, 0.000000000000000000 ) ) ;
#8684=EDGE_CURVE ( 'NONE', #4631, #9513, #6788, .T. ) ;
#8689=DIRECTION ( 'NONE',  ( -0.000000000000000000, -1.000000000000000000, -0.000000000000000000 ) ) ;
#8717=CARTESIAN_POINT ( 'NONE',  ( -0.08413922508867374694, 0.06963377358823465146, 0.006254882657694874927 ) ) ;
#8763=EDGE_CURVE ( 'NONE', #1004, #12588, #13773, .T. ) ;
#8918=VERTEX_POINT ( 'NONE', #8591 ) ;
#8965=ORIENTED_EDGE ( 'NONE', *, *, #6134, .T. ) ;
#8969=ADVANCED_FACE ( 'NONE', ( #7493 ), #1903, .T. ) ;
#9057=CARTESIAN_POINT ( 'NONE',  ( -0.05175539059627463218, 0.07874015748031495954, 0.07475334604056275978 ) ) ;
#9060=EDGE_LOOP ( 'NONE', ( #2744, #11778, #1654, #3551, #9495 ) ) ;
#9076=DIRECTION ( 'NONE',  ( 0.000000000000000000, 0.000000000000000000, 1.000000000000000000 ) ) ;
#9085=CIRCLE ( 'NONE', #15351, 0.03937007874015751446 ) ;
#9105=DIRECTION ( 'NONE',  ( 0.000000000000000000, -0.000000000000000000, 1.000000000000000000 ) ) ;
#9107=CIRCLE ( 'NONE', #2845, 0.003937007874015749712 ) ;
#9108=EDGE_CURVE ( 'NONE', #5548, #8918, #4398, .T. ) ;
#9184=PLANE ( 'NONE',  #3439 ) ;
#9225=EDGE_LOOP ( 'NONE', ( #4440, #10952, #3846, #15365 ) ) ;
#9274=DIRECTION ( 'NONE',  ( 0.000000000000000000, 0.000000000000000000, 1.000000000000000000 ) ) ;
#9277=( NAMED_UNIT ( * ) SI_UNIT ( $, .STERADIAN. ) SOLID_ANGLE_UNIT ( ) );
#9300=CARTESIAN_POINT ( 'NONE',  ( -0.05175539059627463218, 0.07874015748031495954, 0.07475334604056275978 ) ) ;
#9327=ORIENTED_EDGE ( 'NONE', *, *, #5501, .F. ) ;
#9364=FACE_OUTER_BOUND ( 'NONE', #6192, .T. ) ;
#9495=ORIENTED_EDGE ( 'NONE', *, *, #8684, .T. ) ;
#9497=CIRCLE ( 'NONE', #7236, 0.05298991407461853265 ) ;
#9513=VERTEX_POINT ( 'NONE', #10290 ) ;
#9518=( CONVERSION_BASED_UNIT ( 'INCH', #14132 ) LENGTH_UNIT ( ) NAMED_UNIT ( #10560 ) );
#9521=ORIENTED_EDGE ( 'NONE', *, *, #4904, .T. ) ;
#9543=MANIFOLD_SOLID_BREP ( 'Fillet2', #8624 ) ;
#9559=DIRECTION ( 'NONE',  ( 0.000000000000000000, 0.000000000000000000, -1.000000000000000000 ) ) ;
#9566=ORIENTED_EDGE ( 'NONE', *, *, #1746, .F. ) ;
#9603=AXIS2_PLACEMENT_3D ( 'NONE', #8673, #5207, #5444 ) ;
#9650=CIRCLE ( 'NONE', #2873, 0.05298991407461853265 ) ;
#9666=DIRECTION ( 'NONE',  ( 1.000000000000000000, 0.000000000000000000, 1.224646799147353207E-16 ) ) ;
#9695=EDGE_CURVE ( 'NONE', #11304, #161, #7177, .T. ) ;
#9725=DIRECTION ( 'NONE',  ( -0.000000000000000000, 1.000000000000000000, 0.000000000000000000 ) ) ;
#9787=CYLINDRICAL_SURFACE ( 'NONE', #13627, 0.03937007874015751446 ) ;
#9788=ADVANCED_FACE ( 'NONE', ( #5410 ), #9184, .F. ) ;
#9863=VECTOR ( 'NONE', #4602, 39.37007874015748854 ) ;
#9868=DIRECTION ( 'NONE',  ( 0.000000000000000000, 0.000000000000000000, 1.000000000000000000 ) ) ;
#9912=AXIS2_PLACEMENT_3D ( 'NONE', #9057, #13827, #3101 ) ;
#9913=CARTESIAN_POINT ( 'NONE',  ( 0.05175539059627461136, 0.07874015748031495954, -0.07475334604056278753 ) ) ;
#10016=DIRECTION ( 'NONE',  ( 0.000000000000000000, -0.2873478855663456066, -0.9578262852211513190 ) ) ;
#10029=EDGE_CURVE ( 'NONE', #12588, #7658, #7026, .T. ) ;
#10066=FACE_OUTER_BOUND ( 'NONE', #5804, .T. ) ;
#10074=VERTEX_POINT ( 'NONE', #8040 ) ;
#10118=VECTOR ( 'NONE', #2614, 39.37007874015748143 ) ;
#10131=VECTOR ( 'NONE', #745, 39.37007874015748143 ) ;
#10153=CARTESIAN_POINT ( 'NONE',  ( 0.000000000000000000, 0.07480314960629921850, 0.000000000000000000 ) ) ;
#10167=ORIENTED_EDGE ( 'NONE', *, *, #10029, .T. ) ;
#10182=ORIENTED_EDGE ( 'NONE', *, *, #7232, .F. ) ;
#10191=CIRCLE ( 'NONE', #12700, 0.04330708661417326938 ) ;
#10218=SHAPE_DEFINITION_REPRESENTATION ( #914, #2403 ) ;
#10245=CARTESIAN_POINT ( 'NONE',  ( 9.360245101547351149E-18, 0.07093549527207514138, 0.07900545476875124595 ) ) ;
#10248=CARTESIAN_POINT ( 'NONE',  ( 0.03886060139087953863, 0.07874015748031495954, 0.08219815605943972536 ) ) ;
#10278=ADVANCED_FACE ( 'NONE', ( #10066 ), #6378, .F. ) ;
#10281=FACE_BOUND ( 'NONE', #3410, .T. ) ;
#10290=CARTESIAN_POINT ( 'NONE',  ( -0.03886060139087894189, 0.000000000000000000, -0.08219815605944147396 ) ) ;
#10302=CARTESIAN_POINT ( 'NONE',  ( 0.09061599198715353243, 0.06736074103232449206, 0.007444810018878659542 ) ) ;
#10306=ORIENTED_EDGE ( 'NONE', *, *, #15163, .F. ) ;
#10380=LINE ( 'NONE', #12575, #6065 ) ;
#10381=LENGTH_MEASURE_WITH_UNIT ( LENGTH_MEASURE( 0.02539999999999999897 ), #912 );
#10384=FACE_OUTER_BOUND ( 'NONE', #90, .T. ) ;
#10394=ADVANCED_FACE ( 'NONE', ( #10384 ), #2951, .T. ) ;
#10426=CARTESIAN_POINT ( 'NONE',  ( 0.000000000000000000, 0.07874015748031495954, 0.000000000000000000 ) ) ;
#10457=ORIENTED_EDGE ( 'NONE', *, *, #10029, .F. ) ;
#10464=DIRECTION ( 'NONE',  ( 0.000000000000000000, -1.000000000000000000, -0.000000000000000000 ) ) ;
#10513=VERTEX_POINT ( 'NONE', #996 ) ;
#10514=CARTESIAN_POINT ( 'NONE',  ( 0.000000000000000000, 0.003937007874015749712, 0.000000000000000000 ) ) ;
#10538=FACE_OUTER_BOUND ( 'NONE', #4551, .T. ) ;
#10560=DIMENSIONAL_EXPONENTS ( 1.000000000000000000, 0.000000000000000000, 0.000000000000000000, 0.000000000000000000, 0.000000000000000000, 0.000000000000000000, 0.000000000000000000 ) ;
#10652=VECTOR ( 'NONE', #1396, 39.37007874015748854 ) ;
#10671=ORIENTED_EDGE ( 'NONE', *, *, #4908, .T. ) ;
#10674=EDGE_LOOP ( 'NONE', ( #2380, #5971, #5003, #14002 ) ) ;
#10684=LINE ( 'NONE', #3628, #3370 ) ;
#10705=CARTESIAN_POINT ( 'NONE',  ( -0.03886060139087894189, 0.06736074103232447818, -0.08219815605944147396 ) ) ;
#10731=CARTESIAN_POINT ( 'NONE',  ( 0.05175539059627461136, 0.000000000000000000, -0.07475334604056278753 ) ) ;
#10733=DIRECTION ( 'NONE',  ( -0.000000000000000000, -1.000000000000000000, -0.000000000000000000 ) ) ;
#10814=DIRECTION ( 'NONE',  ( -0.000000000000000000, -1.000000000000000000, -0.000000000000000000 ) ) ;
#10952=ORIENTED_EDGE ( 'NONE', *, *, #1943, .T. ) ;
#10962=CARTESIAN_POINT ( 'NONE',  ( 0.000000000000000000, 0.003937007874015749712, 0.000000000000000000 ) ) ;
#11047=CARTESIAN_POINT ( 'NONE',  ( -0.05175539059627463218, 0.06736074103232447818, 0.07475334604056275978 ) ) ;
#11097=DIRECTION ( 'NONE',  ( 0.5692328345973367565, 0.000000000000000000, -0.8221763679505029732 ) ) ;
#11150=AXIS2_PLACEMENT_3D ( 'NONE', #11254, #5362, #14859 ) ;
#11233=LINE ( 'NONE', #4252, #2620 ) ;
#11239=VERTEX_POINT ( 'NONE', #4597 ) ;
#11254=CARTESIAN_POINT ( 'NONE',  ( 0.000000000000000000, 0.000000000000000000, 0.000000000000000000 ) ) ;
#11263=CARTESIAN_POINT ( 'NONE',  ( 0.05823215749475442460, 0.06963377358823460983, -0.06105365336398921317 ) ) ;
#11304=VERTEX_POINT ( 'NONE', #4454 ) ;
#11331=VECTOR ( 'NONE', #11640, 39.37007874015748143 ) ;
#11344=B_SPLINE_CURVE_WITH_KNOTS ( 'NONE', 3,
 ( #10302, #7793, #6611, #11409, #5589 ),
 .UNSPECIFIED., .F., .F.,
 ( 4, 1, 4 ),
 ( 2.432568093614346639E-07, 0.001154943795188590611, 0.002309644333567820521 ),
 .UNSPECIFIED. ) ;
#11361=ORIENTED_EDGE ( 'NONE', *, *, #1196, .T. ) ;
#11385=CARTESIAN_POINT ( 'NONE',  ( 0.03450359373084972703, 0.06995722947081550736, -0.07617071561662594470 ) ) ;
#11390=CARTESIAN_POINT ( 'NONE',  ( 4.821444091131316146E-18, 0.07874015748031495954, 0.03937007874015751446 ) ) ;
#11403=DIRECTION ( 'NONE',  ( 0.000000000000000000, 0.000000000000000000, 1.000000000000000000 ) ) ;
#11409=CARTESIAN_POINT ( 'NONE',  ( 0.04748649982359187671, 0.06963377358818940988, 0.06973926505267954989 ) ) ;
#11422=CARTESIAN_POINT ( 'NONE',  ( 0.03886060139087953863, 0.06736074103232488064, 0.08219815605943972536 ) ) ;
#11442=PRODUCT_DEFINITION_CONTEXT ( 'detailed design', #5986, 'design' ) ;
#11481=AXIS2_PLACEMENT_3D ( 'NONE', #12576, #4264, #5441 ) ;
#11502=DIRECTION ( 'NONE',  ( -0.000000000000000000, -1.000000000000000000, -0.000000000000000000 ) ) ;
#11512=ORIENTED_EDGE ( 'NONE', *, *, #15163, .T. ) ;
#11551=ORIENTED_EDGE ( 'NONE', *, *, #7444, .T. ) ;
#11564=EDGE_LOOP ( 'NONE', ( #7335, #6265 ) ) ;
#11570=DIRECTION ( 'NONE',  ( -0.000000000000000000, -1.000000000000000000, -0.000000000000000000 ) ) ;
#11596=CIRCLE ( 'NONE', #9603, 0.04330708661417326938 ) ;
#11602=DIRECTION ( 'NONE',  ( -0.9040582794047685722, 0.000000000000000000, 0.4274092037376938658 ) ) ;
#11639=CARTESIAN_POINT ( 'NONE',  ( 0.000000000000000000, 0.07874015748031495954, 0.000000000000000000 ) ) ;
#11640=DIRECTION ( 'NONE',  ( -0.000000000000000000, -1.000000000000000000, -0.000000000000000000 ) ) ;
#11647=AXIS2_PLACEMENT_3D ( 'NONE', #15333, #4453, #4521 ) ;
#11663=FACE_OUTER_BOUND ( 'NONE', #7965, .T. ) ;
#11716=EDGE_CURVE ( 'NONE', #8918, #5548, #11596, .T. ) ;
#11726=DIRECTION ( 'NONE',  ( -0.000000000000000000, 1.000000000000000000, 0.000000000000000000 ) ) ;
#11748=EDGE_CURVE ( 'NONE', #10074, #12909, #10380, .T. ) ;
#11778=ORIENTED_EDGE ( 'NONE', *, *, #4244, .T. ) ;
#11797=CARTESIAN_POINT ( 'NONE',  ( 0.000000000000000000, 0.000000000000000000, 0.000000000000000000 ) ) ;
#11806=EDGE_CURVE ( 'NONE', #3700, #9513, #2068, .T. ) ;
#11830=CARTESIAN_POINT ( 'NONE',  ( -0.05175539059627463218, 0.06736074103232447818, 0.07475334604056275978 ) ) ;
#11833=ORIENTED_EDGE ( 'NONE', *, *, #4244, .F. ) ;
#11852=CARTESIAN_POINT ( 'NONE',  ( 6.489392865857486264E-18, 0.07874015748031495954, 0.05298991407461853265 ) ) ;
#11890=ORIENTED_EDGE ( 'NONE', *, *, #7232, .T. ) ;
#11919=AXIS2_PLACEMENT_3D ( 'NONE', #14487, #6158, #3981 ) ;
#11984=CIRCLE ( 'NONE', #12872, 0.003937007874015749712 ) ;
#12144=DIRECTION ( 'NONE',  ( 0.000000000000000000, 0.000000000000000000, -1.000000000000000000 ) ) ;
#12166=DIRECTION ( 'NONE',  ( 1.224646799147353207E-16, 0.000000000000000000, -1.000000000000000000 ) ) ;
#12176=CARTESIAN_POINT ( 'NONE',  ( 5.303588500244447761E-18, 0.07480314960629921850, -0.04330708661417326938 ) ) ;
#12181=EDGE_LOOP ( 'NONE', ( #2466, #7733, #8616, #12943, #12802, #9566, #4512 ) ) ;
#12257=ORIENTED_EDGE ( 'NONE', *, *, #7444, .F. ) ;
#12350=AXIS2_PLACEMENT_3D ( 'NONE', #2055, #4491, #9274 ) ;
#12389=CARTESIAN_POINT ( 'NONE',  ( -0.09061599198715356018, 0.06736074103232447818, -0.007444810018878696839 ) ) ;
#12420=DIRECTION ( 'NONE',  ( 0.000000000000000000, 0.000000000000000000, 1.000000000000000000 ) ) ;
#12575=CARTESIAN_POINT ( 'NONE',  ( 0.09061599198715353243, 0.07874015748031495954, 0.007444810018878659542 ) ) ;
#12576=CARTESIAN_POINT ( 'NONE',  ( 0.000000000000000000, 0.000000000000000000, 0.000000000000000000 ) ) ;
#12588=VERTEX_POINT ( 'NONE', #11830 ) ;
#12644=CARTESIAN_POINT ( 'NONE',  ( 0.01725179686542486351, 0.07136070614489377351, -0.07758808519268911574 ) ) ;
#12700=AXIS2_PLACEMENT_3D ( 'NONE', #14969, #6961, #9076 ) ;
#12726=CARTESIAN_POINT ( 'NONE',  ( 0.000000000000000000, 0.07874015748031495954, 0.000000000000000000 ) ) ;
#12741=ORIENTED_EDGE ( 'NONE', *, *, #6298, .T. ) ;
#12751=EDGE_CURVE ( 'NONE', #7178, #238, #14, .T. ) ;
#12802=ORIENTED_EDGE ( 'NONE', *, *, #6776, .F. ) ;
#12837=CARTESIAN_POINT ( 'NONE',  ( -0.09061599198715356018, 0.000000000000000000, -0.007444810018878696839 ) ) ;
#12872=AXIS2_PLACEMENT_3D ( 'NONE', #6176, #3829, #14661 ) ;
#12885=ORIENTED_EDGE ( 'NONE', *, *, #11716, .F. ) ;
#12895=DIRECTION ( 'NONE',  ( -0.000000000000000000, 1.000000000000000000, 0.000000000000000000 ) ) ;
#12909=VERTEX_POINT ( 'NONE', #2796 ) ;
#12915=CIRCLE ( 'NONE', #2159, 0.03937007874015751446 ) ;
#12943=ORIENTED_EDGE ( 'NONE', *, *, #6298, .F. ) ;
#12957=VERTEX_POINT ( 'NONE', #14076 ) ;
#12975=CARTESIAN_POINT ( 'NONE',  ( -0.03886060139087894189, 0.07874015748031495954, -0.08219815605944147396 ) ) ;
#12990=ADVANCED_FACE ( 'NONE', ( #11663 ), #3891, .T. ) ;
#13012=DIRECTION ( 'NONE',  ( -0.000000000000000000, -1.000000000000000000, -0.000000000000000000 ) ) ;
#13065=DIMENSIONAL_EXPONENTS ( 1.000000000000000000, 0.000000000000000000, 0.000000000000000000, 0.000000000000000000, 0.000000000000000000, 0.000000000000000000, 0.000000000000000000 ) ;
#13103=( LENGTH_UNIT ( ) NAMED_UNIT ( * ) SI_UNIT ( $, .METRE. ) );
#13153=AXIS2_PLACEMENT_3D ( 'NONE', #12726, #4311, #9105 ) ;
#13241=VERTEX_POINT ( 'NONE', #917 ) ;
#13255=CARTESIAN_POINT ( 'NONE',  ( -0.06473829668901623369, 0.07239639532902288066, -0.04482148303916006632 ) ) ;
#13315=CARTESIAN_POINT ( 'NONE',  ( 0.08413922508867374694, 0.06963377358823465146, -0.006254882657694913091 ) ) ;
#13346=LINE ( 'NONE', #9913, #10118 ) ;
#13416=MECHANICAL_DESIGN_GEOMETRIC_PRESENTATION_REPRESENTATION('',(#921),#6644);
#13466=CARTESIAN_POINT ( 'NONE',  ( 0.000000000000000000, 0.07874015748031495954, 0.000000000000000000 ) ) ;
#13513=DIRECTION ( 'NONE',  ( -0.000000000000000000, 1.000000000000000000, 0.000000000000000000 ) ) ;
#13627=AXIS2_PLACEMENT_3D ( 'NONE', #7117, #5939, #12144 ) ;
#13773=B_SPLINE_CURVE_WITH_KNOTS ( 'NONE', 3,
 ( #5765, #4527, #14176, #2260 ),
 .UNSPECIFIED., .F., .F.,
 ( 4, 4 ),
 ( 0.0009905856238791982925, 0.002309601750613628646 ),
 .UNSPECIFIED. ) ;
#13827=DIRECTION ( 'NONE',  ( 0.08188191145424328354, 0.000000000000000000, -0.9966420383350280687 ) ) ;
#13839=B_SPLINE_CURVE_WITH_KNOTS ( 'NONE', 3,
 ( #12389, #1661, #13255, #100, #1341 ),
 .UNSPECIFIED., .F., .F.,
 ( 4, 1, 4 ),
 ( 2.432568093613678012E-07, 0.001154943795188613379, 0.002309644333567865190 ),
 .UNSPECIFIED. ) ;
#13931=AXIS2_PLACEMENT_3D ( 'NONE', #12176, #6035, #5094 ) ;
#13966=ORIENTED_EDGE ( 'NONE', *, *, #8763, .F. ) ;
#13990=DIRECTION ( 'NONE',  ( 0.000000000000000000, -0.000000000000000000, 1.000000000000000000 ) ) ;
#14002=ORIENTED_EDGE ( 'NONE', *, *, #5267, .T. ) ;
#14021=FACE_OUTER_BOUND ( 'NONE', #5577, .T. ) ;
#14067=ORIENTED_EDGE ( 'NONE', *, *, #7517, .T. ) ;
#14076=CARTESIAN_POINT ( 'NONE',  ( 2.419703784132994590E-19, 0.07093549527207483607, -0.07900545476875228679 ) ) ;
#14104=AXIS2_PLACEMENT_3D ( 'NONE', #11639, #10464, #6688 ) ;
#14109=DIRECTION ( 'NONE',  ( 0.4274092037376938102, 0.000000000000000000, 0.9040582794047684612 ) ) ;
#14119=TOROIDAL_SURFACE ( 'NONE', #4322, 0.04330708661417326938, 0.003937007874015747977 ) ;
#14132=LENGTH_MEASURE_WITH_UNIT ( LENGTH_MEASURE( 0.02539999999999999897 ), #13103 );
#14138=ADVANCED_FACE ( 'NONE', ( #14190 ), #3460, .F. ) ;
#14176=CARTESIAN_POINT ( 'NONE',  ( -0.03450359373084976866, 0.06995722947081559062, 0.07617071561662558388 ) ) ;
#14190=FACE_OUTER_BOUND ( 'NONE', #3751, .T. ) ;
#14256=EDGE_LOOP ( 'NONE', ( #1727, #8456 ) ) ;
#14342=EDGE_CURVE ( 'NONE', #2312, #11304, #10191, .T. ) ;
#14370=( NAMED_UNIT ( * ) PLANE_ANGLE_UNIT ( ) SI_UNIT ( $, .RADIAN. ) );
#14380=VECTOR ( 'NONE', #10016, 39.37007874015748854 ) ;
#14382=AXIS2_PLACEMENT_3D ( 'NONE', #6884, #15114, #8146 ) ;
#14399=VECTOR ( 'NONE', #4841, 39.37007874015748143 ) ;
#14487=CARTESIAN_POINT ( 'NONE',  ( 0.000000000000000000, 0.07874015748031495954, 0.000000000000000000 ) ) ;
#14506=ORIENTED_EDGE ( 'NONE', *, *, #8684, .F. ) ;
#14540=VERTEX_POINT ( 'NONE', #7033 ) ;
#14547=DIRECTION ( 'NONE',  ( 0.9966420383350262924, 0.000000000000000000, 0.08188191145426275408 ) ) ;
#14582=CARTESIAN_POINT ( 'NONE',  ( -0.05823215749475443154, 0.06963377358823460983, 0.06105365336398917153 ) ) ;
#14614=CIRCLE ( 'NONE', #14104, 0.04330708661417326938 ) ;
#14632=LINE ( 'NONE', #6289, #10652 ) ;
#14661=DIRECTION ( 'NONE',  ( 0.000000000000000000, 0.000000000000000000, 1.000000000000000000 ) ) ;
#14684=ORIENTED_EDGE ( 'NONE', *, *, #2072, .T. ) ;
#14747=UNCERTAINTY_MEASURE_WITH_UNIT (LENGTH_MEASURE( 1.000000000000000082E-05 ), #9518, 'distance_accuracy_value', 'NONE');
#14793=ORIENTED_EDGE ( 'NONE', *, *, #9695, .F. ) ;
#14859=DIRECTION ( 'NONE',  ( 0.000000000000000000, 0.000000000000000000, 1.000000000000000000 ) ) ;
#14872=CARTESIAN_POINT ( 'NONE',  ( 0.09061599198715353243, 0.06736074103232449206, 0.007444810018878659542 ) ) ;
#14913=VECTOR ( 'NONE', #8049, 39.37007874015748143 ) ;
#14969=CARTESIAN_POINT ( 'NONE',  ( 0.000000000000000000, 0.07874015748031495954, 0.000000000000000000 ) ) ;
#15020=PLANE ( 'NONE',  #9912 ) ;
#15060=PLANE ( 'NONE',  #13153 ) ;
#15114=DIRECTION ( 'NONE',  ( 0.9040582794047686832, 0.000000000000000000, -0.4274092037376937547 ) ) ;
#15163=EDGE_CURVE ( 'NONE', #2312, #13241, #11984, .T. ) ;
#15165=( CONVERSION_BASED_UNIT ( 'INCH', #10381 ) LENGTH_UNIT ( ) NAMED_UNIT ( #13065 ) );
#15199=VECTOR ( 'NONE', #11570, 39.37007874015748143 ) ;
#15246=( NAMED_UNIT ( * ) SI_UNIT ( $, .STERADIAN. ) SOLID_ANGLE_UNIT ( ) );
#15299=DIRECTION ( 'NONE',  ( 1.172998894335282758E-16, -0.2873478855663456066, 0.9578262852211513190 ) ) ;
#15315=FACE_OUTER_BOUND ( 'NONE', #3302, .T. ) ;
#15333=CARTESIAN_POINT ( 'NONE',  ( 0.000000000000000000, 0.07874015748031495954, 0.000000000000000000 ) ) ;
#15351=AXIS2_PLACEMENT_3D ( 'NONE', #7247, #6049, #5910 ) ;
#15365=ORIENTED_EDGE ( 'NONE', *, *, #7517, .F. ) ;
#15402=DIRECTION ( 'NONE',  ( -0.000000000000000000, 1.000000000000000000, 0.000000000000000000 ) ) ;
#15439=AXIS2_PLACEMENT_3D ( 'NONE', #8238, #13012, #3226 ) ;
#15455=AXIS2_PLACEMENT_3D ( 'NONE', #4867, #9666, #12166 ) ;
#15527=COLOUR_RGB('Black',0.12,0.14,0.17);
#15528=FILL_AREA_STYLE_COLOUR('',#15527);
#15529=FILL_AREA_STYLE('',(#15528));
#15530=SURFACE_STYLE_FILL_AREA(#15529);
#15531=SURFACE_SIDE_STYLE('',(#15530));
#15532=SURFACE_STYLE_USAGE(.BOTH.,#15531);
#15533=PRESENTATION_STYLE_ASSIGNMENT((#15532));
ENDSEC;
END-ISO-10303-21;
